ISO-10303-21;
HEADER;
/* Generated by software containing ST-Developer
 * from STEP Tools, Inc. (www.steptools.com) 
 */

FILE_DESCRIPTION(
/* description */ ('STEP AP214'),
/* implementation_level */ '2;1');

FILE_NAME(
/* name */ 'Coupling Washer.step',
/* time_stamp */ '2026-11-15T14:49:54-08:00',
/* author */ (''),
/* organization */ (''),
/* preprocessor_version */ 'ST-DEVELOPER v20.2',
/* originating_system */ 'Autodesk Translation Framework v15.17.0.0',
/* authorisation */ '');

FILE_SCHEMA (('AUTOMOTIVE_DESIGN { 1 0 10303 214 3 1 1 }'));
ENDSEC;

DATA;
#10=MECHANICAL_DESIGN_GEOMETRIC_PRESENTATION_REPRESENTATION('',(#1121),#66721);
#1058=SHAPE_REPRESENTATION_RELATIONSHIP('SRR','None',#66921,#1089);
#1089=ADVANCED_BREP_SHAPE_REPRESENTATION('',(#1156),#66712);
#1121=STYLED_ITEM('',(#67095),#1156);
#1156=MANIFOLD_SOLID_BREP('Body1',#25687);
#1427=FACE_BOUND('',#5155,.T.);
#2119=PLANE('',#28210);
#2120=PLANE('',#28212);
#2121=PLANE('',#28215);
#2122=PLANE('',#28216);
#2123=PLANE('',#28217);
#2124=PLANE('',#28218);
#2125=PLANE('',#28219);
#2126=PLANE('',#28220);
#2127=PLANE('',#28221);
#3453=FACE_OUTER_BOUND('',#5154,.T.);
#3454=FACE_OUTER_BOUND('',#5156,.T.);
#3455=FACE_OUTER_BOUND('',#5157,.T.);
#3456=FACE_OUTER_BOUND('',#5158,.T.);
#3457=FACE_OUTER_BOUND('',#5159,.T.);
#3458=FACE_OUTER_BOUND('',#5160,.T.);
#3459=FACE_OUTER_BOUND('',#5161,.T.);
#3460=FACE_OUTER_BOUND('',#5162,.T.);
#3461=FACE_OUTER_BOUND('',#5163,.T.);
#3462=FACE_OUTER_BOUND('',#5164,.T.);
#5154=EDGE_LOOP('',(#22610));
#5155=EDGE_LOOP('',(#22611,#22612,#22613,#22614,#22615,#22616));
#5156=EDGE_LOOP('',(#22617));
#5157=EDGE_LOOP('',(#22618,#22619,#22620,#22621));
#5158=EDGE_LOOP('',(#22622,#22623,#22624,#22625,#22626,#22627));
#5159=EDGE_LOOP('',(#22628,#22629,#22630,#22631));
#5160=EDGE_LOOP('',(#22632,#22633,#22634,#22635));
#5161=EDGE_LOOP('',(#22636,#22637,#22638,#22639));
#5162=EDGE_LOOP('',(#22640,#22641,#22642,#22643));
#5163=EDGE_LOOP('',(#22644,#22645,#22646,#22647));
#5164=EDGE_LOOP('',(#22648,#22649,#22650,#22651));
#7105=LINE('',#65031,#9094);
#7106=LINE('',#65033,#9095);
#7107=LINE('',#65035,#9096);
#7108=LINE('',#65037,#9097);
#7109=LINE('',#65039,#9098);
#7110=LINE('',#65040,#9099);
#7111=LINE('',#65045,#9100);
#7112=LINE('',#65049,#9101);
#7113=LINE('',#65051,#9102);
#7114=LINE('',#65053,#9103);
#7115=LINE('',#65055,#9104);
#7116=LINE('',#65057,#9105);
#7117=LINE('',#65058,#9106);
#7118=LINE('',#65060,#9107);
#7119=LINE('',#65061,#9108);
#7120=LINE('',#65063,#9109);
#7121=LINE('',#65065,#9110);
#7122=LINE('',#65067,#9111);
#7123=LINE('',#65069,#9112);
#9094=VECTOR('',#34720,1000.);
#9095=VECTOR('',#34721,1000.);
#9096=VECTOR('',#34722,1000.);
#9097=VECTOR('',#34723,1000.);
#9098=VECTOR('',#34724,1000.);
#9099=VECTOR('',#34725,1000.);
#9100=VECTOR('',#34732,2.5);
#9101=VECTOR('',#34735,1000.);
#9102=VECTOR('',#34736,1000.);
#9103=VECTOR('',#34737,1000.);
#9104=VECTOR('',#34738,1000.);
#9105=VECTOR('',#34739,1000.);
#9106=VECTOR('',#34740,1000.);
#9107=VECTOR('',#34743,1000.);
#9108=VECTOR('',#34744,1000.);
#9109=VECTOR('',#34747,1000.);
#9110=VECTOR('',#34750,1000.);
#9111=VECTOR('',#34753,1000.);
#9112=VECTOR('',#34756,1000.);
#10443=CIRCLE('',#28211,2.5);
#10444=CIRCLE('',#28213,2.5);
#12589=VERTEX_POINT('',#65027);
#12590=VERTEX_POINT('',#65029);
#12591=VERTEX_POINT('',#65030);
#12592=VERTEX_POINT('',#65032);
#12593=VERTEX_POINT('',#65034);
#12594=VERTEX_POINT('',#65036);
#12595=VERTEX_POINT('',#65038);
#12596=VERTEX_POINT('',#65042);
#12597=VERTEX_POINT('',#65047);
#12598=VERTEX_POINT('',#65048);
#12599=VERTEX_POINT('',#65050);
#12600=VERTEX_POINT('',#65052);
#12601=VERTEX_POINT('',#65054);
#12602=VERTEX_POINT('',#65056);
#15998=EDGE_CURVE('',#12589,#12589,#10443,.T.);
#15999=EDGE_CURVE('',#12590,#12591,#7105,.T.);
#16000=EDGE_CURVE('',#12591,#12592,#7106,.T.);
#16001=EDGE_CURVE('',#12592,#12593,#7107,.T.);
#16002=EDGE_CURVE('',#12593,#12594,#7108,.T.);
#16003=EDGE_CURVE('',#12594,#12595,#7109,.T.);
#16004=EDGE_CURVE('',#12595,#12590,#7110,.T.);
#16005=EDGE_CURVE('',#12596,#12596,#10444,.T.);
#16006=EDGE_CURVE('',#12589,#12596,#7111,.T.);
#16007=EDGE_CURVE('',#12597,#12598,#7112,.T.);
#16008=EDGE_CURVE('',#12599,#12597,#7113,.T.);
#16009=EDGE_CURVE('',#12600,#12599,#7114,.T.);
#16010=EDGE_CURVE('',#12601,#12600,#7115,.T.);
#16011=EDGE_CURVE('',#12602,#12601,#7116,.T.);
#16012=EDGE_CURVE('',#12598,#12602,#7117,.T.);
#16013=EDGE_CURVE('',#12597,#12595,#7118,.T.);
#16014=EDGE_CURVE('',#12598,#12590,#7119,.T.);
#16015=EDGE_CURVE('',#12599,#12594,#7120,.T.);
#16016=EDGE_CURVE('',#12600,#12593,#7121,.T.);
#16017=EDGE_CURVE('',#12601,#12592,#7122,.T.);
#16018=EDGE_CURVE('',#12602,#12591,#7123,.T.);
#22610=ORIENTED_EDGE('',*,*,#15998,.T.);
#22611=ORIENTED_EDGE('',*,*,#15999,.T.);
#22612=ORIENTED_EDGE('',*,*,#16000,.T.);
#22613=ORIENTED_EDGE('',*,*,#16001,.T.);
#22614=ORIENTED_EDGE('',*,*,#16002,.T.);
#22615=ORIENTED_EDGE('',*,*,#16003,.T.);
#22616=ORIENTED_EDGE('',*,*,#16004,.T.);
#22617=ORIENTED_EDGE('',*,*,#16005,.T.);
#22618=ORIENTED_EDGE('',*,*,#15998,.F.);
#22619=ORIENTED_EDGE('',*,*,#16006,.T.);
#22620=ORIENTED_EDGE('',*,*,#16005,.F.);
#22621=ORIENTED_EDGE('',*,*,#16006,.F.);
#22622=ORIENTED_EDGE('',*,*,#16007,.F.);
#22623=ORIENTED_EDGE('',*,*,#16008,.F.);
#22624=ORIENTED_EDGE('',*,*,#16009,.F.);
#22625=ORIENTED_EDGE('',*,*,#16010,.F.);
#22626=ORIENTED_EDGE('',*,*,#16011,.F.);
#22627=ORIENTED_EDGE('',*,*,#16012,.F.);
#22628=ORIENTED_EDGE('',*,*,#16004,.F.);
#22629=ORIENTED_EDGE('',*,*,#16013,.F.);
#22630=ORIENTED_EDGE('',*,*,#16007,.T.);
#22631=ORIENTED_EDGE('',*,*,#16014,.T.);
#22632=ORIENTED_EDGE('',*,*,#16003,.F.);
#22633=ORIENTED_EDGE('',*,*,#16015,.F.);
#22634=ORIENTED_EDGE('',*,*,#16008,.T.);
#22635=ORIENTED_EDGE('',*,*,#16013,.T.);
#22636=ORIENTED_EDGE('',*,*,#16002,.F.);
#22637=ORIENTED_EDGE('',*,*,#16016,.F.);
#22638=ORIENTED_EDGE('',*,*,#16009,.T.);
#22639=ORIENTED_EDGE('',*,*,#16015,.T.);
#22640=ORIENTED_EDGE('',*,*,#16001,.F.);
#22641=ORIENTED_EDGE('',*,*,#16017,.F.);
#22642=ORIENTED_EDGE('',*,*,#16010,.T.);
#22643=ORIENTED_EDGE('',*,*,#16016,.T.);
#22644=ORIENTED_EDGE('',*,*,#16000,.F.);
#22645=ORIENTED_EDGE('',*,*,#16018,.F.);
#22646=ORIENTED_EDGE('',*,*,#16011,.T.);
#22647=ORIENTED_EDGE('',*,*,#16017,.T.);
#22648=ORIENTED_EDGE('',*,*,#15999,.F.);
#22649=ORIENTED_EDGE('',*,*,#16014,.F.);
#22650=ORIENTED_EDGE('',*,*,#16012,.T.);
#22651=ORIENTED_EDGE('',*,*,#16018,.T.);
#24143=CYLINDRICAL_SURFACE('',#28214,2.5);
#25406=ADVANCED_FACE('',(#3453,#1427),#2119,.T.);
#25407=ADVANCED_FACE('',(#3454),#2120,.T.);
#25408=ADVANCED_FACE('',(#3455),#24143,.T.);
#25409=ADVANCED_FACE('',(#3456),#2121,.F.);
#25410=ADVANCED_FACE('',(#3457),#2122,.F.);
#25411=ADVANCED_FACE('',(#3458),#2123,.F.);
#25412=ADVANCED_FACE('',(#3459),#2124,.F.);
#25413=ADVANCED_FACE('',(#3460),#2125,.F.);
#25414=ADVANCED_FACE('',(#3461),#2126,.F.);
#25415=ADVANCED_FACE('',(#3462),#2127,.F.);
#25687=CLOSED_SHELL('',(#25406,#25407,#25408,#25409,#25410,#25411,#25412,
#25413,#25414,#25415));
#28209=AXIS2_PLACEMENT_3D('',#65025,#34714,#34715);
#28210=AXIS2_PLACEMENT_3D('',#65026,#34716,#34717);
#28211=AXIS2_PLACEMENT_3D('',#65028,#34718,#34719);
#28212=AXIS2_PLACEMENT_3D('',#65041,#34726,#34727);
#28213=AXIS2_PLACEMENT_3D('',#65043,#34728,#34729);
#28214=AXIS2_PLACEMENT_3D('',#65044,#34730,#34731);
#28215=AXIS2_PLACEMENT_3D('',#65046,#34733,#34734);
#28216=AXIS2_PLACEMENT_3D('',#65059,#34741,#34742);
#28217=AXIS2_PLACEMENT_3D('',#65062,#34745,#34746);
#28218=AXIS2_PLACEMENT_3D('',#65064,#34748,#34749);
#28219=AXIS2_PLACEMENT_3D('',#65066,#34751,#34752);
#28220=AXIS2_PLACEMENT_3D('',#65068,#34754,#34755);
#28221=AXIS2_PLACEMENT_3D('',#65070,#34757,#34758);
#34714=DIRECTION('axis',(0.,0.,1.));
#34715=DIRECTION('refdir',(1.,0.,0.));
#34716=DIRECTION('center_axis',(0.,0.707106781186548,0.707106781186548));
#34717=DIRECTION('ref_axis',(1.,0.,0.));
#34718=DIRECTION('center_axis',(0.,0.707106781186548,0.707106781186548));
#34719=DIRECTION('ref_axis',(1.,0.,0.));
#34720=DIRECTION('',(0.866025403761799,-0.353553390621002,0.353553390621002));
#34721=DIRECTION('',(0.,-0.707106781186547,0.707106781186547));
#34722=DIRECTION('',(-0.866025403761799,-0.353553390621002,0.353553390621002));
#34723=DIRECTION('',(-0.866025403761799,0.353553390621002,-0.353553390621002));
#34724=DIRECTION('',(0.,0.707106781186547,-0.707106781186547));
#34725=DIRECTION('',(0.866025403761799,0.353553390621002,-0.353553390621002));
#34726=DIRECTION('center_axis',(0.,-0.707106781186548,-0.707106781186548));
#34727=DIRECTION('ref_axis',(0.,-0.707106781186548,0.707106781186548));
#34728=DIRECTION('center_axis',(0.,-0.707106781186548,-0.707106781186548));
#34729=DIRECTION('ref_axis',(1.,0.,0.));
#34730=DIRECTION('center_axis',(0.,0.707106781186548,0.707106781186548));
#34731=DIRECTION('ref_axis',(1.,0.,0.));
#34732=DIRECTION('',(0.,-0.707106781186548,-0.707106781186548));
#34733=DIRECTION('center_axis',(0.,-0.707106781186547,-0.707106781186548));
#34734=DIRECTION('ref_axis',(0.,-0.707106781186548,0.707106781186547));
#34735=DIRECTION('',(0.866025403761798,0.353553390621003,-0.353553390621002));
#34736=DIRECTION('',(0.,0.707106781186548,-0.707106781186547));
#34737=DIRECTION('',(-0.866025403761798,0.353553390621003,-0.353553390621002));
#34738=DIRECTION('',(-0.866025403761798,-0.353553390621003,0.353553390621002));
#34739=DIRECTION('',(0.,-0.707106781186548,0.707106781186547));
#34740=DIRECTION('',(0.866025403761798,-0.353553390621003,0.353553390621002));
#34741=DIRECTION('center_axis',(-0.500000000039214,0.612372435679786,-0.612372435679785));
#34742=DIRECTION('ref_axis',(-0.774596669209083,-2.65897497434893E-17,0.632455532073358));
#34743=DIRECTION('',(0.,0.707106781186547,0.707106781186548));
#34744=DIRECTION('',(0.,0.707106781186547,0.707106781186548));
#34745=DIRECTION('center_axis',(-1.,0.,0.));
#34746=DIRECTION('ref_axis',(0.,0.,1.));
#34747=DIRECTION('',(0.,0.707106781186547,0.707106781186548));
#34748=DIRECTION('center_axis',(-0.500000000039214,-0.612372435679786,0.612372435679785));
#34749=DIRECTION('ref_axis',(-0.774596669209084,0.632455532073357,1.86150232200487E-17));
#34750=DIRECTION('',(0.,0.707106781186547,0.707106781186548));
#34751=DIRECTION('center_axis',(0.500000000039214,-0.612372435679786,0.612372435679785));
#34752=DIRECTION('ref_axis',(-0.774596669209084,-0.632455532073357,-1.86150232200487E-17));
#34753=DIRECTION('',(0.,0.707106781186547,0.707106781186548));
#34754=DIRECTION('center_axis',(1.,0.,0.));
#34755=DIRECTION('ref_axis',(0.,1.,0.));
#34756=DIRECTION('',(0.,0.707106781186547,0.707106781186548));
#34757=DIRECTION('center_axis',(0.500000000039214,0.612372435679786,-0.612372435679785));
#34758=DIRECTION('ref_axis',(-0.774596669209083,2.65897497434893E-17,-0.632455532073358));
#65025=CARTESIAN_POINT('',(0.,0.,0.));
#65026=CARTESIAN_POINT('Origin',(-29.,17.1826947828386,17.1826947828386));
#65027=CARTESIAN_POINT('',(-31.5,17.1826947828386,17.1826947828386));
#65028=CARTESIAN_POINT('Origin',(-29.,17.1826947828386,17.1826947828386));
#65029=CARTESIAN_POINT('',(-29.,18.1624906800114,16.2028988857214));
#65030=CARTESIAN_POINT('',(-27.8,17.6725927314035,16.6927968343292));
#65031=CARTESIAN_POINT('',(-28.3999999999746,17.9175417056693,16.4478478600079));
#65032=CARTESIAN_POINT('',(-27.8,16.6927968343292,17.6725927314035));
#65033=CARTESIAN_POINT('',(-27.8,17.0602202957321,17.3051692700007));
#65034=CARTESIAN_POINT('',(-29.,16.2028988857213,18.1624906800114));
#65035=CARTESIAN_POINT('',(-28.3999999999746,16.4478478600079,17.9175417056693));
#65036=CARTESIAN_POINT('',(-30.2,16.6927968343292,17.6725927314035));
#65037=CARTESIAN_POINT('',(-29.6000000000254,16.4478478600079,17.9175417056693));
#65038=CARTESIAN_POINT('',(-30.2,17.6725927314035,16.6927968343292));
#65039=CARTESIAN_POINT('',(-30.2,17.1826947828664,17.1826947828664));
#65040=CARTESIAN_POINT('',(-29.6000000000254,17.9175417056693,16.4478478600079));
#65041=CARTESIAN_POINT('Origin',(-29.,8.6974134086,8.6974134086));
#65042=CARTESIAN_POINT('',(-31.5,8.6974134086,8.6974134086));
#65043=CARTESIAN_POINT('Origin',(-29.,8.6974134086,8.6974134086));
#65044=CARTESIAN_POINT('Origin',(-29.,12.9400540957193,12.9400540957193));
#65045=CARTESIAN_POINT('',(-31.5,12.9400540957193,12.9400540957193));
#65046=CARTESIAN_POINT('Origin',(-29.,15.4149278299,15.4149278299));
#65047=CARTESIAN_POINT('',(-30.2,15.9048257784372,14.9250298813628));
#65048=CARTESIAN_POINT('',(-29.,16.394723727045,14.435131932755));
#65049=CARTESIAN_POINT('',(-30.2,15.9048257784372,14.9250298813628));
#65050=CARTESIAN_POINT('',(-30.2,14.9250298813628,15.9048257784372));
#65051=CARTESIAN_POINT('',(-30.2,14.9250298813628,15.9048257784372));
#65052=CARTESIAN_POINT('',(-29.,14.435131932755,16.394723727045));
#65053=CARTESIAN_POINT('',(-29.,14.435131932755,16.394723727045));
#65054=CARTESIAN_POINT('',(-27.8,14.9250298813628,15.9048257784372));
#65055=CARTESIAN_POINT('',(-27.8,14.9250298813628,15.9048257784372));
#65056=CARTESIAN_POINT('',(-27.8,15.9048257784372,14.9250298813628));
#65057=CARTESIAN_POINT('',(-27.8,15.9048257784372,14.9250298813628));
#65058=CARTESIAN_POINT('',(-29.,16.394723727045,14.435131932755));
#65059=CARTESIAN_POINT('Origin',(-29.6,16.1497747527411,14.6800809070589));
#65060=CARTESIAN_POINT('',(-30.2,15.9048257784372,14.9250298813628));
#65061=CARTESIAN_POINT('',(-29.,16.394723727045,14.435131932755));
#65062=CARTESIAN_POINT('Origin',(-30.2,15.4149278299,15.4149278299));
#65063=CARTESIAN_POINT('',(-30.2,14.9250298813628,15.9048257784372));
#65064=CARTESIAN_POINT('Origin',(-29.6,14.6800809070589,16.1497747527411));
#65065=CARTESIAN_POINT('',(-29.,14.435131932755,16.394723727045));
#65066=CARTESIAN_POINT('Origin',(-28.4,14.6800809070589,16.1497747527411));
#65067=CARTESIAN_POINT('',(-27.8,14.9250298813628,15.9048257784372));
#65068=CARTESIAN_POINT('Origin',(-27.8,15.1699788556314,15.6598768041686));
#65069=CARTESIAN_POINT('',(-27.8,15.9048257784372,14.9250298813628));
#65070=CARTESIAN_POINT('Origin',(-28.4,16.1497747527411,14.6800809070589));
#66671=UNCERTAINTY_MEASURE_WITH_UNIT(LENGTH_MEASURE(0.01),#66722,
'DISTANCE_ACCURACY_VALUE',
'Maximum model space distance between geometric entities at asserted c
onnectivities');
#66680=UNCERTAINTY_MEASURE_WITH_UNIT(LENGTH_MEASURE(0.01),#66722,
'DISTANCE_ACCURACY_VALUE',
'Maximum model space distance between geometric entities at asserted c
onnectivities');
#66712=(
GEOMETRIC_REPRESENTATION_CONTEXT(3)
GLOBAL_UNCERTAINTY_ASSIGNED_CONTEXT((#66671))
GLOBAL_UNIT_ASSIGNED_CONTEXT((#66722,#66724,#66725))
REPRESENTATION_CONTEXT('','3D')
);
#66721=(
GEOMETRIC_REPRESENTATION_CONTEXT(3)
GLOBAL_UNCERTAINTY_ASSIGNED_CONTEXT((#66680))
GLOBAL_UNIT_ASSIGNED_CONTEXT((#66722,#66724,#66725))
REPRESENTATION_CONTEXT('','3D')
);
#66722=(
LENGTH_UNIT()
NAMED_UNIT(*)
SI_UNIT(.MILLI.,.METRE.)
);
#66724=(
NAMED_UNIT(*)
PLANE_ANGLE_UNIT()
SI_UNIT($,.RADIAN.)
);
#66725=(
NAMED_UNIT(*)
SI_UNIT($,.STERADIAN.)
SOLID_ANGLE_UNIT()
);
#66757=SHAPE_DEFINITION_REPRESENTATION(#66817,#66921);
#66817=PRODUCT_DEFINITION_SHAPE('',$,#66962);
#66921=SHAPE_REPRESENTATION('',(#28209),#66712);
#66930=PRODUCT_DEFINITION_CONTEXT('part definition',#67052,'design');
#66962=PRODUCT_DEFINITION('Coupling Washer','Coupling Washer',#67002,#66930);
#67002=PRODUCT_DEFINITION_FORMATION('',$,#67085);
#67052=APPLICATION_CONTEXT(
'Core Data for Automotive Mechanical Design Process');
#67053=PRODUCT_CONTEXT('part definition',#67052,'mechanical');
#67085=PRODUCT('Coupling Washer','Coupling Washer',$,(#67053));
#67095=PRESENTATION_STYLE_ASSIGNMENT((#67097));
#67097=SURFACE_STYLE_USAGE(.BOTH.,#67099);
#67099=SURFACE_SIDE_STYLE('',(#67101));
#67101=SURFACE_STYLE_FILL_AREA(#67103);
#67103=FILL_AREA_STYLE('Opaque(202,209,238)',(#67105));
#67105=FILL_AREA_STYLE_COLOUR('Opaque(202,209,238)',#67107);
#67107=COLOUR_RGB('Opaque(202,209,238)',0.792156862745098,0.819607843137255,
0.933333333333333);
ENDSEC;
END-ISO-10303-21;
